ISO-10303-21;
HEADER;
FILE_DESCRIPTION (('STEP AP214'),
    '1' );
FILE_NAME ('socket head cap screw_iso_ISO 4762 M5 x 16 - 16N.step',
    '2026-10-23T15:04:32',
    ( '' ),
    ( '' ),
    'SwSTEP 2.0',
    'SolidWorks 2026',
    '' );
FILE_SCHEMA (( 'AUTOMOTIVE_DESIGN' ));
ENDSEC;

DATA;
#1=AXIS2_PLACEMENT_3D ( 'NONE', #713, #1643, #1457 ) ;
#3=AXIS2_PLACEMENT_3D ( 'NONE', #402, #1764, #2101 ) ;
#4=VERTEX_POINT ( 'NONE', #2115 ) ;
#8=PLANE ( 'NONE',  #1813 ) ;
#11=DIRECTION ( 'NONE',  ( 0.000000000000000000, 0.5000000000000009992, 0.8660254037844380415 ) ) ;
#13=EDGE_CURVE ( 'NONE', #1816, #847, #1494, .T. ) ;
#17=DIRECTION ( 'NONE',  ( 1.000000000000000000, 0.000000000000000000, 0.000000000000000000 ) ) ;
#23=VECTOR ( 'NONE', #1974, 1000.000000000000000 ) ;
#28=DIRECTION ( 'NONE',  ( 0.000000000000000000, -0.5000000000000009992, -0.8660254037844380415 ) ) ;
#30=AXIS2_PLACEMENT_3D ( 'NONE', #971, #1660, #79 ) ;
#34=VECTOR ( 'NONE', #1991, 1000.000000000000000 ) ;
#37=CARTESIAN_POINT ( 'NONE',  ( 2.500000000000000000, 2.357898499370431722, -2.818925648462311528E-15 ) ) ;
#40=EDGE_CURVE ( 'NONE', #1625, #1348, #636, .T. ) ;
#54=ORIENTED_EDGE ( 'NONE', *, *, #1804, .F. ) ;
#55=EDGE_CURVE ( 'NONE', #1358, #1353, #1429, .T. ) ;
#58=CARTESIAN_POINT ( 'NONE',  ( 0.000000000000000000, -1.178949249685214307, 2.042000000000001592 ) ) ;
#65=VERTEX_POINT ( 'NONE', #648 ) ;
#75=CARTESIAN_POINT ( 'NONE',  ( 2.500000000000000000, 1.178949249685212974, -2.042000000000001148 ) ) ;
#76=DIRECTION ( 'NONE',  ( 0.000000000000000000, 0.000000000000000000, 1.000000000000000000 ) ) ;
#79=DIRECTION ( 'NONE',  ( 1.000000000000000000, 0.000000000000000000, 0.000000000000000000 ) ) ;
#80=VERTEX_POINT ( 'NONE', #828 ) ;
#84=ORIENTED_EDGE ( 'NONE', *, *, #604, .T. ) ;
#85=DIRECTION ( 'NONE',  ( 1.000000000000000000, 0.000000000000000000, 0.000000000000000000 ) ) ;
#86=ORIENTED_EDGE ( 'NONE', *, *, #306, .T. ) ;
#91=VECTOR ( 'NONE', #730, 1000.000000000000114 ) ;
#95=EDGE_LOOP ( 'NONE', ( #1914, #1029, #1402 ) ) ;
#101=EDGE_CURVE ( 'NONE', #1631, #537, #2026, .T. ) ;
#105=CARTESIAN_POINT ( 'NONE',  ( 2.500000000000000000, 0.000000000000000000, 0.000000000000000000 ) ) ;
#110=ORIENTED_EDGE ( 'NONE', *, *, #318, .F. ) ;
#115=ADVANCED_FACE ( 'NONE', ( #2005 ), #793, .T. ) ;
#123=ORIENTED_EDGE ( 'NONE', *, *, #401, .T. ) ;
#126=CARTESIAN_POINT ( 'NONE',  ( 21.00000000000000355, 0.000000000000000000, 0.000000000000000000 ) ) ;
#132=ADVANCED_FACE ( 'NONE', ( #2209 ), #2220, .F. ) ;
#133=ORIENTED_EDGE ( 'NONE', *, *, #586, .T. ) ;
#136=ORIENTED_EDGE ( 'NONE', *, *, #518, .T. ) ;
#138=DIRECTION ( 'NONE',  ( 1.000000000000000000, 0.000000000000000000, 0.000000000000000000 ) ) ;
#139=CIRCLE ( 'NONE', #605, 2.500000000000000444 ) ;
#140=EDGE_LOOP ( 'NONE', ( #2012, #1805, #2066, #1757, #813 ) ) ;
#141=DIRECTION ( 'NONE',  ( 0.000000000000000000, 0.000000000000000000, -1.000000000000000000 ) ) ;
#143=SURFACE_SIDE_STYLE ('',( #858 ) ) ;
#144=EDGE_CURVE ( 'NONE', #1505, #145, #1507, .T. ) ;
#145=VERTEX_POINT ( 'NONE', #489 ) ;
#149=CARTESIAN_POINT ( 'NONE',  ( 0.2500000000000002220, 0.000000000000000000, 0.000000000000000000 ) ) ;
#150=CARTESIAN_POINT ( 'NONE',  ( 2.500000000000000000, 2.357898499370431722, -2.818925648462311528E-15 ) ) ;
#153=DIRECTION ( 'NONE',  ( 0.000000000000000000, -1.000000000000000000, 0.000000000000000000 ) ) ;
#156=AXIS2_PLACEMENT_3D ( 'NONE', #1101, #1761, #935 ) ;
#157=ORIENTED_EDGE ( 'NONE', *, *, #401, .F. ) ;
#162=EDGE_LOOP ( 'NONE', ( #1939, #248, #188, #677 ) ) ;
#163=CARTESIAN_POINT ( 'NONE',  ( -31.74999999999995737, 0.000000000000000000, 0.000000000000000000 ) ) ;
#164=CARTESIAN_POINT ( 'NONE',  ( 5.200000000000002842, 0.000000000000000000, 2.500000000000000444 ) ) ;
#165=EDGE_CURVE ( 'NONE', #314, #2053, #1896, .T. ) ;
#172=EDGE_LOOP ( 'NONE', ( #1456, #1524 ) ) ;
#180=EDGE_CURVE ( 'NONE', #226, #627, #965, .T. ) ;
#183=AXIS2_PLACEMENT_3D ( 'NONE', #2092, #526, #1052 ) ;
#184=ADVANCED_FACE ( 'NONE', ( #1232 ), #388, .T. ) ;
#188=ORIENTED_EDGE ( 'NONE', *, *, #880, .T. ) ;
#189=CARTESIAN_POINT ( 'NONE',  ( 5.200000000000002842, 0.000000000000000000, 0.000000000000000000 ) ) ;
#190=DIRECTION ( 'NONE',  ( 0.000000000000000000, -0.4999999999999989453, 0.8660254037844391517 ) ) ;
#192=DIRECTION ( 'NONE',  ( -1.000000000000000000, -0.000000000000000000, -0.000000000000000000 ) ) ;
#193=LINE ( 'NONE', #908, #1216 ) ;
#195=ORIENTED_EDGE ( 'NONE', *, *, #283, .T. ) ;
#196=CARTESIAN_POINT ( 'NONE',  ( 2.500000000000000000, 1.178949249685212974, -2.042000000000001148 ) ) ;
#200=CARTESIAN_POINT ( 'NONE',  ( 5.200000000000002842, 0.000000000000000000, 0.000000000000000000 ) ) ;
#201=DIRECTION ( 'NONE',  ( -1.000000000000000000, -0.000000000000000000, -0.000000000000000000 ) ) ;
#206=ORIENTED_EDGE ( 'NONE', *, *, #1935, .T. ) ;
#207=DIRECTION ( 'NONE',  ( 1.000000000000000000, 0.000000000000000000, 0.000000000000000000 ) ) ;
#209=DIRECTION ( 'NONE',  ( 0.000000000000000000, 0.000000000000000000, -1.000000000000000000 ) ) ;
#212=CARTESIAN_POINT ( 'NONE',  ( 2.500000000000000000, -2.357898499370432166, 3.035766082959412415E-15 ) ) ;
#220=VERTEX_POINT ( 'NONE', #2089 ) ;
#224=EDGE_CURVE ( 'NONE', #575, #1831, #600, .T. ) ;
#226=VERTEX_POINT ( 'NONE', #357 ) ;
#228=LINE ( 'NONE', #585, #1036 ) ;
#232=EDGE_CURVE ( 'NONE', #65, #2053, #1572, .T. ) ;
#233=CIRCLE ( 'NONE', #866, 4.250000000000000000 ) ;
#236=CARTESIAN_POINT ( 'NONE',  ( 3.678949249685231848, 0.000000000000000000, 0.000000000000000000 ) ) ;
#239=CARTESIAN_POINT ( 'NONE',  ( 2.500000000000000000, 2.357898499370431722, -2.818925648462311528E-15 ) ) ;
#248=ORIENTED_EDGE ( 'NONE', *, *, #706, .T. ) ;
#249=ORIENTED_EDGE ( 'NONE', *, *, #424, .F. ) ;
#254=CIRCLE ( 'NONE', #3, 4.000000000000000000 ) ;
#255=VECTOR ( 'NONE', #2191, 1000.000000000000000 ) ;
#270=EDGE_LOOP ( 'NONE', ( #655, #206, #1374 ) ) ;
#271=LINE ( 'NONE', #1566, #1453 ) ;
#274=AXIS2_PLACEMENT_3D ( 'NONE', #873, #679, #190 ) ;
#277=AXIS2_PLACEMENT_3D ( 'NONE', #538, #1561, #1211 ) ;
#283=EDGE_CURVE ( 'NONE', #1794, #1470, #1533, .T. ) ;
#285=ORIENTED_EDGE ( 'NONE', *, *, #1767, .T. ) ;
#286=AXIS2_PLACEMENT_3D ( 'NONE', #1522, #857, #1497 ) ;
#288=DIRECTION ( 'NONE',  ( 0.000000000000000000, -0.5000000000000013323, -0.8660254037844380415 ) ) ;
#290=CLOSED_SHELL ( 'NONE', ( #1208, #1730, #801, #1062, #184, #534, #1347, #1500, #1560, #469, #1546, #374, #979, #115, #1267, #2103, #1607, #1259, #869, #1380, #531, #1775, #1016, #132, #451, #1373, #1562 ) ) ;
#292=CARTESIAN_POINT ( 'NONE',  ( 0.000000000000000000, -2.357898499370432166, 3.035766082959412415E-15 ) ) ;
#293=CARTESIAN_POINT ( 'NONE',  ( 2.500000000000000000, 1.178949249685217415, 2.041999999999998483 ) ) ;
#295=DIRECTION ( 'NONE',  ( 0.000000000000000000, -0.5000000000000009992, -0.8660254037844380415 ) ) ;
#297=( GEOMETRIC_REPRESENTATION_CONTEXT ( 3 ) GLOBAL_UNCERTAINTY_ASSIGNED_CONTEXT ( ( #1869 ) ) GLOBAL_UNIT_ASSIGNED_CONTEXT ( ( #1381, #1558, #1182 ) ) REPRESENTATION_CONTEXT ( 'NONE', 'WORKASPACE' ) );
#301=CARTESIAN_POINT ( 'NONE',  ( 2.500000000000000000, 0.000000000000000000, 0.000000000000000000 ) ) ;
#302=AXIS2_PLACEMENT_3D ( 'NONE', #75, #1797, #1080 ) ;
#303=CARTESIAN_POINT ( 'NONE',  ( 2.500000000000000000, 1.178949249685212974, -2.042000000000001148 ) ) ;
#304=DIRECTION ( 'NONE',  ( -1.000000000000000000, -0.000000000000000000, -0.000000000000000000 ) ) ;
#306=EDGE_CURVE ( 'NONE', #4, #1672, #1360, .T. ) ;
#312=CARTESIAN_POINT ( 'NONE',  ( 0.000000000000000000, 0.000000000000000000, 0.000000000000000000 ) ) ;
#314=VERTEX_POINT ( 'NONE', #236 ) ;
#316=CIRCLE ( 'NONE', #1206, 2.500000000000000888 ) ;
#318=EDGE_CURVE ( 'NONE', #2053, #1816, #228, .T. ) ;
#319=PRESENTATION_STYLE_ASSIGNMENT (( #1548 ) ) ;
#320=APPLICATION_CONTEXT ( 'automotive_design' ) ;
#322=ORIENTED_EDGE ( 'NONE', *, *, #1708, .F. ) ;
#325=DIRECTION ( 'NONE',  ( -1.000000000000000000, -0.000000000000000000, -0.000000000000000000 ) ) ;
#327=AXIS2_PLACEMENT_3D ( 'NONE', #1511, #1026, #1679 ) ;
#329=FACE_OUTER_BOUND ( 'NONE', #1684, .T. ) ;
#338=VECTOR ( 'NONE', #28, 1000.000000000000114 ) ;
#349=EDGE_LOOP ( 'NONE', ( #249, #593, #1950, #1766 ) ) ;
#354=SHAPE_REPRESENTATION ( 'socket head cap screw_iso_ISO 4762 M5 x 16 - 16N', ( #30 ), #1018 ) ;
#357=CARTESIAN_POINT ( 'NONE',  ( 5.000000000000002665, 0.000000000000000000, -2.700000000000000622 ) ) ;
#360=CARTESIAN_POINT ( 'NONE',  ( 2.500000000000000000, 1.768423874527822459, -1.021000000000002794 ) ) ;
#364=ORIENTED_EDGE ( 'NONE', *, *, #1034, .F. ) ;
#368=FACE_OUTER_BOUND ( 'NONE', #1880, .T. ) ;
#370=VECTOR ( 'NONE', #446, 1000.000000000000000 ) ;
#371=DIRECTION ( 'NONE',  ( 0.000000000000000000, -0.5000000000000013323, -0.8660254037844380415 ) ) ;
#374=ADVANCED_FACE ( 'NONE', ( #1128 ), #1994, .T. ) ;
#378=EDGE_CURVE ( 'NONE', #220, #830, #1795, .T. ) ;
#380=LINE ( 'NONE', #554, #722 ) ;
#382=DIRECTION ( 'NONE',  ( 1.000000000000000000, 0.000000000000000000, 0.000000000000000000 ) ) ;
#384=EDGE_CURVE ( 'NONE', #463, #1794, #597, .T. ) ;
#388=CYLINDRICAL_SURFACE ( 'NONE', #1179, 2.500000000000000444 ) ;
#391=AXIS2_PLACEMENT_3D ( 'NONE', #2068, #2060, #524 ) ;
#393=FACE_OUTER_BOUND ( 'NONE', #1768, .T. ) ;
#400=FACE_OUTER_BOUND ( 'NONE', #1537, .T. ) ;
#401=EDGE_CURVE ( 'NONE', #314, #575, #271, .T. ) ;
#402=CARTESIAN_POINT ( 'NONE',  ( 0.000000000000000000, 0.000000000000000000, 0.000000000000000000 ) ) ;
#405=VERTEX_POINT ( 'NONE', #555 ) ;
#406=AXIS2_PLACEMENT_3D ( 'NONE', #490, #999, #818 ) ;
#410=CARTESIAN_POINT ( 'NONE',  ( 2.500000000000000000, -1.178949249685214307, 2.042000000000001592 ) ) ;
#411=EDGE_LOOP ( 'NONE', ( #157, #890, #1925, #1517, #285 ) ) ;
#413=DIRECTION ( 'NONE',  ( -1.000000000000000000, -0.000000000000000000, -0.000000000000000000 ) ) ;
#424=EDGE_CURVE ( 'NONE', #2192, #4, #546, .T. ) ;
#425=PRODUCT_DEFINITION_SHAPE ( 'NONE', 'NONE',  #1410 ) ;
#430=ORIENTED_EDGE ( 'NONE', *, *, #1751, .F. ) ;
#431=APPLICATION_CONTEXT ( 'automotive_design' ) ;
#432=ORIENTED_EDGE ( 'NONE', *, *, #775, .T. ) ;
#435=DIRECTION ( 'NONE',  ( -0.5000000000000051070, 0.000000000000000000, 0.8660254037844355990 ) ) ;
#439=CARTESIAN_POINT ( 'NONE',  ( 2.500000000000000000, 0.000000000000000000, 0.000000000000000000 ) ) ;
#442=ORIENTED_EDGE ( 'NONE', *, *, #775, .F. ) ;
#444=CIRCLE ( 'NONE', #2022, 0.2000000000000000944 ) ;
#446=DIRECTION ( 'NONE',  ( -1.000000000000000000, -0.000000000000000000, -0.000000000000000000 ) ) ;
#451=ADVANCED_FACE ( 'NONE', ( #393 ), #1399, .F. ) ;
#452=ORIENTED_EDGE ( 'NONE', *, *, #101, .T. ) ;
#454=ORIENTED_EDGE ( 'NONE', *, *, #1956, .T. ) ;
#460=( NAMED_UNIT ( * ) SI_UNIT ( $, .STERADIAN. ) SOLID_ANGLE_UNIT ( ) );
#463=VERTEX_POINT ( 'NONE', #1616 ) ;
#464=CARTESIAN_POINT ( 'NONE',  ( 2.500000000000000000, 0.000000000000000000, 0.000000000000000000 ) ) ;
#468=DIRECTION ( 'NONE',  ( 0.000000000000000000, 0.000000000000000000, -1.000000000000000000 ) ) ;
#469=ADVANCED_FACE ( 'NONE', ( #782 ), #2081, .T. ) ;
#470=CARTESIAN_POINT ( 'NONE',  ( 5.000000000000002665, 3.306546357697854226E-16, 2.700000000000000622 ) ) ;
#478=CIRCLE ( 'NONE', #1724, 0.2500000000000002220 ) ;
#480=VECTOR ( 'NONE', #596, 1000.000000000000000 ) ;
#481=CARTESIAN_POINT ( 'NONE',  ( 0.2500000000000002220, 0.000000000000000000, 0.000000000000000000 ) ) ;
#488=ORIENTED_EDGE ( 'NONE', *, *, #2122, .T. ) ;
#489=CARTESIAN_POINT ( 'NONE',  ( 0.000000000000000000, 1.178949249685212974, -2.042000000000001148 ) ) ;
#490=CARTESIAN_POINT ( 'NONE',  ( 2.500000000000000000, 0.000000000000000000, 0.000000000000000000 ) ) ;
#493=CONICAL_SURFACE ( 'NONE', #1919, 2.055000000000000160, 0.7853981633974639331 ) ;
#499=DIRECTION ( 'NONE',  ( -1.000000000000000000, -0.000000000000000000, -0.000000000000000000 ) ) ;
#503=ORIENTED_EDGE ( 'NONE', *, *, #1309, .T. ) ;
#504=CARTESIAN_POINT ( 'NONE',  ( 0.2500000000000002220, 0.000000000000000000, 4.000000000000000000 ) ) ;
#505=CARTESIAN_POINT ( 'NONE',  ( 5.200000000000002842, 0.000000000000000000, 0.000000000000000000 ) ) ;
#514=MECHANICAL_DESIGN_GEOMETRIC_PRESENTATION_REPRESENTATION('',(#1549),#297);
#515=ORIENTED_EDGE ( 'NONE', *, *, #1804, .T. ) ;
#518=EDGE_CURVE ( 'NONE', #1097, #1470, #611, .T. ) ;
#524=DIRECTION ( 'NONE',  ( 0.000000000000000000, 0.000000000000000000, -1.000000000000000000 ) ) ;
#525=DIRECTION ( 'NONE',  ( -1.000000000000000000, -0.000000000000000000, -0.000000000000000000 ) ) ;
#526=DIRECTION ( 'NONE',  ( -1.000000000000000000, -0.000000000000000000, -0.000000000000000000 ) ) ;
#531=ADVANCED_FACE ( 'NONE', ( #1140 ), #1335, .F. ) ;
#534=ADVANCED_FACE ( 'NONE', ( #329 ), #855, .T. ) ;
#535=CARTESIAN_POINT ( 'NONE',  ( 2.500000000000000000, -1.178949249685214307, 2.042000000000001592 ) ) ;
#537=VERTEX_POINT ( 'NONE', #292 ) ;
#538=CARTESIAN_POINT ( 'NONE',  ( 2.500000000000000000, 0.000000000000000000, 0.000000000000000000 ) ) ;
#546=LINE ( 'NONE', #1743, #1551 ) ;
#547=CARTESIAN_POINT ( 'NONE',  ( 2.500000000000000000, -1.178949249685214307, 2.042000000000001592 ) ) ;
#549=ORIENTED_EDGE ( 'NONE', *, *, #616, .T. ) ;
#551=DIRECTION ( 'NONE',  ( 0.000000000000000000, -1.000000000000000000, 1.287488025362403787E-15 ) ) ;
#554=CARTESIAN_POINT ( 'NONE',  ( -31.74999999999995737, 0.000000000000000000, 4.250000000000000000 ) ) ;
#555=CARTESIAN_POINT ( 'NONE',  ( 4.999999999999997335, 0.000000000000000000, 4.250000000000000000 ) ) ;
#556=CARTESIAN_POINT ( 'NONE',  ( 2.500000000000000000, 1.178949249685217415, 2.041999999999998483 ) ) ;
#558=ORIENTED_EDGE ( 'NONE', *, *, #378, .F. ) ;
#562=CARTESIAN_POINT ( 'NONE',  ( 21.00000000000000355, 2.789133085058097101E-16, -2.055000000000000160 ) ) ;
#563=LINE ( 'NONE', #410, #1905 ) ;
#565=PLANE ( 'NONE',  #302 ) ;
#570=AXIS2_PLACEMENT_3D ( 'NONE', #912, #1927, #1770 ) ;
#575=VERTEX_POINT ( 'NONE', #2029 ) ;
#576=LINE ( 'NONE', #1260, #2086 ) ;
#578=PLANE ( 'NONE',  #1787 ) ;
#584=ORIENTED_EDGE ( 'NONE', *, *, #55, .T. ) ;
#585=CARTESIAN_POINT ( 'NONE',  ( 2.500000000000000000, 1.178949249685212974, -2.042000000000001148 ) ) ;
#586=EDGE_CURVE ( 'NONE', #1579, #80, #478, .T. ) ;
#587=DIRECTION ( 'NONE',  ( 0.000000000000000000, 0.8660254037844380415, -0.5000000000000012212 ) ) ;
#591=DIRECTION ( 'NONE',  ( 0.000000000000000000, 0.000000000000000000, 1.000000000000000000 ) ) ;
#593=ORIENTED_EDGE ( 'NONE', *, *, #2015, .T. ) ;
#596=DIRECTION ( 'NONE',  ( 0.000000000000000000, 1.000000000000000000, -1.287488025362403787E-15 ) ) ;
#597=LINE ( 'NONE', #1968, #1856 ) ;
#600=CIRCLE ( 'NONE', #277, 2.041999999999999815 ) ;
#602=CARTESIAN_POINT ( 'NONE',  ( 5.200000000000002842, 3.061616997868383634E-16, -2.500000000000000444 ) ) ;
#604=EDGE_CURVE ( 'NONE', #776, #1816, #1996, .T. ) ;
#605=AXIS2_PLACEMENT_3D ( 'NONE', #505, #17, #2030 ) ;
#608=CARTESIAN_POINT ( 'NONE',  ( 5.200000000000002842, 0.000000000000000000, -2.700000000000000622 ) ) ;
#609=CARTESIAN_POINT ( 'NONE',  ( 4.999999999999997335, 0.000000000000000000, 0.000000000000000000 ) ) ;
#611=LINE ( 'NONE', #1980, #370 ) ;
#614=CARTESIAN_POINT ( 'NONE',  ( 5.000000000000000888, 4.250000000000000000, 0.000000000000000000 ) ) ;
#616=EDGE_CURVE ( 'NONE', #65, #145, #672, .T. ) ;
#618=( LENGTH_UNIT ( ) NAMED_UNIT ( * ) SI_UNIT ( .MILLI., .METRE. ) );
#620=COLOUR_RGB ( '',1.000000000000000000, 0.9490196078431372140, 0.9098039215686274384 ) ;
#622=EDGE_LOOP ( 'NONE', ( #2158, #682, #110, #1343, #549 ) ) ;
#624=AXIS2_PLACEMENT_3D ( 'NONE', #481, #138, #2017 ) ;
#627=VERTEX_POINT ( 'NONE', #470 ) ;
#628=LINE ( 'NONE', #1308, #2032 ) ;
#629=DIRECTION ( 'NONE',  ( -1.000000000000000000, -0.000000000000000000, -0.000000000000000000 ) ) ;
#636=LINE ( 'NONE', #1138, #1369 ) ;
#637=FACE_OUTER_BOUND ( 'NONE', #933, .T. ) ;
#648=CARTESIAN_POINT ( 'NONE',  ( 2.500000000000000000, 1.178949249685212974, -2.042000000000001148 ) ) ;
#649=DIRECTION ( 'NONE',  ( 0.000000000000000000, 0.000000000000000000, 1.000000000000000000 ) ) ;
#655=ORIENTED_EDGE ( 'NONE', *, *, #2083, .F. ) ;
#660=DIRECTION ( 'NONE',  ( -1.000000000000000000, -0.000000000000000000, -0.000000000000000000 ) ) ;
#661=ORIENTED_EDGE ( 'NONE', *, *, #424, .T. ) ;
#662=DIRECTION ( 'NONE',  ( -1.000000000000000000, -0.000000000000000000, -0.000000000000000000 ) ) ;
#664=( NAMED_UNIT ( * ) PLANE_ANGLE_UNIT ( ) SI_UNIT ( $, .RADIAN. ) );
#666=LINE ( 'NONE', #1830, #1584 ) ;
#670=EDGE_CURVE ( 'NONE', #575, #1569, #809, .T. ) ;
#672=LINE ( 'NONE', #303, #1619 ) ;
#673=CONICAL_SURFACE ( 'NONE', #1774, 2.041999999999999815, 1.047197551196591858 ) ;
#676=EDGE_LOOP ( 'NONE', ( #430, #86, #1552, #1065 ) ) ;
#677=ORIENTED_EDGE ( 'NONE', *, *, #879, .F. ) ;
#678=DIRECTION ( 'NONE',  ( 0.000000000000000000, 0.000000000000000000, 1.000000000000000000 ) ) ;
#679=DIRECTION ( 'NONE',  ( -0.000000000000000000, 0.8660254037844392627, 0.4999999999999990008 ) ) ;
#682=ORIENTED_EDGE ( 'NONE', *, *, #13, .F. ) ;
#685=AXIS2_PLACEMENT_3D ( 'NONE', #778, #2119, #209 ) ;
#688=ORIENTED_EDGE ( 'NONE', *, *, #1935, .F. ) ;
#690=FACE_OUTER_BOUND ( 'NONE', #1015, .T. ) ;
#692=DIRECTION ( 'NONE',  ( 1.000000000000000000, 0.000000000000000000, 0.000000000000000000 ) ) ;
#699=DIRECTION ( 'NONE',  ( 0.000000000000000000, -0.8660254037844390407, -0.4999999999999993339 ) ) ;
#706=EDGE_CURVE ( 'NONE', #1353, #1358, #1157, .T. ) ;
#711=CARTESIAN_POINT ( 'NONE',  ( 0.000000000000000000, -1.178949249685214307, 2.042000000000001592 ) ) ;
#713=CARTESIAN_POINT ( 'NONE',  ( -31.74999999999995737, 0.000000000000000000, 0.000000000000000000 ) ) ;
#715=EDGE_LOOP ( 'NONE', ( #1004, #870, #1543 ) ) ;
#720=DIRECTION ( 'NONE',  ( 0.000000000000000000, 0.000000000000000000, -1.000000000000000000 ) ) ;
#722=VECTOR ( 'NONE', #1033, 1000.000000000000000 ) ;
#729=ORIENTED_EDGE ( 'NONE', *, *, #1681, .F. ) ;
#730=DIRECTION ( 'NONE',  ( -0.5000000000000051070, 1.060575238724903217E-16, -0.8660254037844355990 ) ) ;
#731=DIRECTION ( 'NONE',  ( 0.000000000000000000, -1.000000000000000000, 0.000000000000000000 ) ) ;
#740=DIRECTION ( 'NONE',  ( -1.000000000000000000, -0.000000000000000000, -0.000000000000000000 ) ) ;
#743=DIRECTION ( 'NONE',  ( -0.7071067811865364705, 0.000000000000000000, 0.7071067811865584529 ) ) ;
#746=EDGE_CURVE ( 'NONE', #220, #1505, #1729, .T. ) ;
#750=CONICAL_SURFACE ( 'NONE', #977, 2.041999999999999815, 1.047197551196591858 ) ;
#753=FACE_OUTER_BOUND ( 'NONE', #95, .T. ) ;
#755=ORIENTED_EDGE ( 'NONE', *, *, #604, .F. ) ;
#757=FACE_OUTER_BOUND ( 'NONE', #162, .T. ) ;
#764=DIRECTION ( 'NONE',  ( 0.000000000000000000, -0.5000000000000009992, -0.8660254037844380415 ) ) ;
#765=EDGE_CURVE ( 'NONE', #405, #1579, #380, .T. ) ;
#769=ORIENTED_EDGE ( 'NONE', *, *, #283, .F. ) ;
#773=PRODUCT_CONTEXT ( 'NONE', #320, 'mechanical' ) ;
#775=EDGE_CURVE ( 'NONE', #1348, #537, #1235, .T. ) ;
#776=VERTEX_POINT ( 'NONE', #1069 ) ;
#778=CARTESIAN_POINT ( 'NONE',  ( 2.500000000000000000, 2.357898499370431722, -2.818925648462311528E-15 ) ) ;
#782=FACE_OUTER_BOUND ( 'NONE', #1808, .T. ) ;
#790=ORIENTED_EDGE ( 'NONE', *, *, #144, .F. ) ;
#793=TOROIDAL_SURFACE ( 'NONE', #1252, 4.000000000000000000, 0.2500000000000000000 ) ;
#796=ORIENTED_EDGE ( 'NONE', *, *, #101, .F. ) ;
#798=DIRECTION ( 'NONE',  ( -1.000000000000000000, -0.000000000000000000, -0.000000000000000000 ) ) ;
#799=LINE ( 'NONE', #293, #23 ) ;
#801=ADVANCED_FACE ( 'NONE', ( #368 ), #944, .F. ) ;
#804=TOROIDAL_SURFACE ( 'NONE', #2123, 2.700000000000000622, 0.2000000000000000111 ) ;
#809=LINE ( 'NONE', #1871, #1902 ) ;
#810=LINE ( 'NONE', #2127, #825 ) ;
#813=ORIENTED_EDGE ( 'NONE', *, *, #1708, .T. ) ;
#814=LINE ( 'NONE', #974, #1051 ) ;
#815=ORIENTED_EDGE ( 'NONE', *, *, #1007, .F. ) ;
#818=DIRECTION ( 'NONE',  ( 0.000000000000000000, 0.000000000000000000, 1.000000000000000000 ) ) ;
#820=DIRECTION ( 'NONE',  ( 0.000000000000000000, 0.000000000000000000, -1.000000000000000000 ) ) ;
#824=ORIENTED_EDGE ( 'NONE', *, *, #2083, .T. ) ;
#825=VECTOR ( 'NONE', #1987, 1000.000000000000114 ) ;
#828=CARTESIAN_POINT ( 'NONE',  ( 0.000000000000000000, 0.000000000000000000, 4.000000000000000000 ) ) ;
#830=VERTEX_POINT ( 'NONE', #360 ) ;
#836=PRODUCT_DEFINITION_FORMATION_WITH_SPECIFIED_SOURCE ( 'ANY', '', #967, .NOT_KNOWN. ) ;
#840=CIRCLE ( 'NONE', #1408, 4.250000000000000000 ) ;
#844=CARTESIAN_POINT ( 'NONE',  ( 2.500000000000000000, 2.357898499370431722, -2.818925648462311528E-15 ) ) ;
#847=VERTEX_POINT ( 'NONE', #1207 ) ;
#851=DIRECTION ( 'NONE',  ( -1.000000000000000000, -0.000000000000000000, -0.000000000000000000 ) ) ;
#852=DIRECTION ( 'NONE',  ( -1.000000000000000000, -0.000000000000000000, -0.000000000000000000 ) ) ;
#855=CYLINDRICAL_SURFACE ( 'NONE', #1050, 4.250000000000000000 ) ;
#856=CIRCLE ( 'NONE', #2065, 0.2000000000000000944 ) ;
#857=DIRECTION ( 'NONE',  ( 1.000000000000000000, 0.000000000000000000, 0.000000000000000000 ) ) ;
#858=SURFACE_STYLE_FILL_AREA ( #1362 ) ;
#861=ORIENTED_EDGE ( 'NONE', *, *, #2166, .T. ) ;
#866=AXIS2_PLACEMENT_3D ( 'NONE', #2099, #740, #924 ) ;
#869=ADVANCED_FACE ( 'NONE', ( #1116 ), #565, .F. ) ;
#870=ORIENTED_EDGE ( 'NONE', *, *, #1956, .F. ) ;
#871=EDGE_LOOP ( 'NONE', ( #488, #1641, #432, #921, #1341, #790 ) ) ;
#873=CARTESIAN_POINT ( 'NONE',  ( 2.500000000000000000, -2.357898499370432166, 3.035766082959412415E-15 ) ) ;
#879=EDGE_CURVE ( 'NONE', #1097, #463, #2057, .T. ) ;
#880=EDGE_CURVE ( 'NONE', #1358, #463, #576, .T. ) ;
#881=ORIENTED_EDGE ( 'NONE', *, *, #224, .T. ) ;
#884=DIRECTION ( 'NONE',  ( -1.000000000000000000, -0.000000000000000000, -0.000000000000000000 ) ) ;
#890=ORIENTED_EDGE ( 'NONE', *, *, #165, .T. ) ;
#891=CARTESIAN_POINT ( 'NONE',  ( 2.500000000000000000, 2.500728763858895382E-16, -2.041999999999999815 ) ) ;
#894=CARTESIAN_POINT ( 'NONE',  ( 2.500000000000000000, 2.357898499370431722, -2.818925648462311528E-15 ) ) ;
#895=CIRCLE ( 'NONE', #327, 2.041999999999999815 ) ;
#900=DIRECTION ( 'NONE',  ( 0.000000000000000000, 0.000000000000000000, 1.000000000000000000 ) ) ;
#908=CARTESIAN_POINT ( 'NONE',  ( 2.500000000000000000, 2.357898499370431722, -2.818925648462311528E-15 ) ) ;
#909=ORIENTED_EDGE ( 'NONE', *, *, #966, .T. ) ;
#912=CARTESIAN_POINT ( 'NONE',  ( 0.000000000000000000, 0.000000000000000000, 0.000000000000000000 ) ) ;
#915=ORIENTED_EDGE ( 'NONE', *, *, #40, .F. ) ;
#920=CIRCLE ( 'NONE', #1173, 2.041999999999999815 ) ;
#921=ORIENTED_EDGE ( 'NONE', *, *, #1077, .T. ) ;
#924=DIRECTION ( 'NONE',  ( 0.000000000000000000, 0.000000000000000000, 1.000000000000000000 ) ) ;
#926=VECTOR ( 'NONE', #551, 1000.000000000000000 ) ;
#933=EDGE_LOOP ( 'NONE', ( #584, #861, #1975, #1295 ) ) ;
#935=DIRECTION ( 'NONE',  ( 0.000000000000000000, -1.000000000000000000, 1.287488025362403787E-15 ) ) ;
#937=EDGE_LOOP ( 'NONE', ( #1629, #1796 ) ) ;
#938=PLANE ( 'NONE',  #1932 ) ;
#944=TOROIDAL_SURFACE ( 'NONE', #1407, 2.700000000000000622, 0.2000000000000000111 ) ;
#948=LINE ( 'NONE', #37, #1541 ) ;
#950=EDGE_LOOP ( 'NONE', ( #973, #1636 ) ) ;
#957=VERTEX_POINT ( 'NONE', #1418 ) ;
#959=CARTESIAN_POINT ( 'NONE',  ( 4.999999999999997335, 5.204748896376250699E-16, -4.250000000000000000 ) ) ;
#960=ORIENTED_EDGE ( 'NONE', *, *, #1077, .F. ) ;
#961=DIRECTION ( 'NONE',  ( 0.000000000000000000, 0.000000000000000000, -1.000000000000000000 ) ) ;
#965=CIRCLE ( 'NONE', #391, 2.700000000000000622 ) ;
#966=EDGE_CURVE ( 'NONE', #1672, #80, #254, .T. ) ;
#967=PRODUCT ( 'socket head cap screw_iso_ISO 4762 M5 x 16 - 16N', 'socket head cap screw_iso_ISO 4762 M5 x 16 - 16N', '', ( #773 ) ) ;
#968=FACE_BOUND ( 'NONE', #937, .T. ) ;
#970=SHAPE_DEFINITION_REPRESENTATION ( #425, #354 ) ;
#971=CARTESIAN_POINT ( 'NONE',  ( 0.000000000000000000, 0.000000000000000000, 0.000000000000000000 ) ) ;
#972=( GEOMETRIC_REPRESENTATION_CONTEXT ( 3 ) GLOBAL_UNCERTAINTY_ASSIGNED_CONTEXT ( ( #1529 ) ) GLOBAL_UNIT_ASSIGNED_CONTEXT ( ( #1311, #1997, #460 ) ) REPRESENTATION_CONTEXT ( 'NONE', 'WORKASPACE' ) );
#973=ORIENTED_EDGE ( 'NONE', *, *, #1363, .F. ) ;
#974=CARTESIAN_POINT ( 'NONE',  ( 21.00000000000000355, 2.516649172247811061E-16, -2.055000000000000160 ) ) ;
#975=ORIENTED_EDGE ( 'NONE', *, *, #1973, .T. ) ;
#977=AXIS2_PLACEMENT_3D ( 'NONE', #105, #798, #1765 ) ;
#979=ADVANCED_FACE ( 'NONE', ( #1010 ), #804, .F. ) ;
#990=DIRECTION ( 'NONE',  ( -1.000000000000000000, -0.000000000000000000, -0.000000000000000000 ) ) ;
#992=DIRECTION ( 'NONE',  ( 0.000000000000000000, 1.000000000000000000, -1.287488025362403787E-15 ) ) ;
#993=EDGE_CURVE ( 'NONE', #80, #1672, #1984, .T. ) ;
#994=ORIENTED_EDGE ( 'NONE', *, *, #1992, .T. ) ;
#998=DIRECTION ( 'NONE',  ( 1.000000000000000000, 0.000000000000000000, 0.000000000000000000 ) ) ;
#999=DIRECTION ( 'NONE',  ( -1.000000000000000000, -0.000000000000000000, -0.000000000000000000 ) ) ;
#1001=DIRECTION ( 'NONE',  ( 1.000000000000000000, 0.000000000000000000, 0.000000000000000000 ) ) ;
#1004=ORIENTED_EDGE ( 'NONE', *, *, #1712, .F. ) ;
#1007=EDGE_CURVE ( 'NONE', #2053, #776, #1376, .T. ) ;
#1008=ORIENTED_EDGE ( 'NONE', *, *, #966, .F. ) ;
#1010=FACE_OUTER_BOUND ( 'NONE', #2135, .T. ) ;
#1015=EDGE_LOOP ( 'NONE', ( #960, #796, #2059, #84, #1520 ) ) ;
#1016=ADVANCED_FACE ( 'NONE', ( #1845 ), #1676, .F. ) ;
#1018=( GEOMETRIC_REPRESENTATION_CONTEXT ( 3 ) GLOBAL_UNCERTAINTY_ASSIGNED_CONTEXT ( ( #1357 ) ) GLOBAL_UNIT_ASSIGNED_CONTEXT ( ( #618, #664, #2203 ) ) REPRESENTATION_CONTEXT ( 'NONE', 'WORKASPACE' ) );
#1020=DIRECTION ( 'NONE',  ( -1.000000000000000000, -0.000000000000000000, -0.000000000000000000 ) ) ;
#1021=AXIS2_PLACEMENT_3D ( 'NONE', #1953, #2146, #1247 ) ;
#1026=DIRECTION ( 'NONE',  ( -1.000000000000000000, -0.000000000000000000, -0.000000000000000000 ) ) ;
#1029=ORIENTED_EDGE ( 'NONE', *, *, #232, .T. ) ;
#1032=ORIENTED_EDGE ( 'NONE', *, *, #224, .F. ) ;
#1033=DIRECTION ( 'NONE',  ( -1.000000000000000000, -0.000000000000000000, -0.000000000000000000 ) ) ;
#1034=EDGE_CURVE ( 'NONE', #1579, #4, #1224, .T. ) ;
#1036=VECTOR ( 'NONE', #1591, 1000.000000000000000 ) ;
#1050=AXIS2_PLACEMENT_3D ( 'NONE', #163, #662, #2200 ) ;
#1051=VECTOR ( 'NONE', #1467, 1000.000000000000114 ) ;
#1052=DIRECTION ( 'NONE',  ( 0.000000000000000000, 0.000000000000000000, 1.000000000000000000 ) ) ;
#1062=ADVANCED_FACE ( 'NONE', ( #637 ), #493, .T. ) ;
#1063=VECTOR ( 'NONE', #288, 999.9999999999997726 ) ;
#1065=ORIENTED_EDGE ( 'NONE', *, *, #586, .F. ) ;
#1067=DIRECTION ( 'NONE',  ( 0.000000000000000000, -0.4999999999999993339, 0.8660254037844390407 ) ) ;
#1069=CARTESIAN_POINT ( 'NONE',  ( 2.500000000000000000, -1.768423874527825568, -1.020999999999998575 ) ) ;
#1073=AXIS2_PLACEMENT_3D ( 'NONE', #1698, #998, #1675 ) ;
#1077=EDGE_CURVE ( 'NONE', #537, #847, #1858, .T. ) ;
#1079=DIRECTION ( 'NONE',  ( 0.000000000000000000, 0.000000000000000000, 1.000000000000000000 ) ) ;
#1080=DIRECTION ( 'NONE',  ( 0.000000000000000000, 1.000000000000000000, -1.287488025362403787E-15 ) ) ;
#1088=DIRECTION ( 'NONE',  ( 0.000000000000000000, -1.224646799147353454E-16, 1.000000000000000000 ) ) ;
#1089=FACE_OUTER_BOUND ( 'NONE', #2035, .T. ) ;
#1097=VERTEX_POINT ( 'NONE', #1833 ) ;
#1098=ORIENTED_EDGE ( 'NONE', *, *, #670, .F. ) ;
#1099=CARTESIAN_POINT ( 'NONE',  ( 0.2500000000000002220, 4.898587196589412829E-16, -4.000000000000000000 ) ) ;
#1101=CARTESIAN_POINT ( 'NONE',  ( 2.500000000000000000, -1.178949249685214307, 2.042000000000001592 ) ) ;
#1102=ORIENTED_EDGE ( 'NONE', *, *, #306, .F. ) ;
#1103=EDGE_CURVE ( 'NONE', #830, #2053, #920, .T. ) ;
#1105=AXIS2_PLACEMENT_3D ( 'NONE', #1958, #1786, #1623 ) ;
#1112=PLANE ( 'NONE',  #1894 ) ;
#1116=FACE_OUTER_BOUND ( 'NONE', #622, .T. ) ;
#1118=DIRECTION ( 'NONE',  ( -1.000000000000000000, -0.000000000000000000, -0.000000000000000000 ) ) ;
#1120=VECTOR ( 'NONE', #884, 1000.000000000000000 ) ;
#1124=ORIENTED_EDGE ( 'NONE', *, *, #378, .T. ) ;
#1128=FACE_OUTER_BOUND ( 'NONE', #172, .T. ) ;
#1131=DIRECTION ( 'NONE',  ( 0.000000000000000000, 0.000000000000000000, -1.000000000000000000 ) ) ;
#1138=CARTESIAN_POINT ( 'NONE',  ( 2.500000000000000000, -1.178949249685214307, 2.042000000000001592 ) ) ;
#1140=FACE_OUTER_BOUND ( 'NONE', #1617, .T. ) ;
#1141=FACE_OUTER_BOUND ( 'NONE', #676, .T. ) ;
#1143=EDGE_CURVE ( 'NONE', #220, #1831, #628, .T. ) ;
#1148=AXIS2_PLACEMENT_3D ( 'NONE', #126, #499, #678 ) ;
#1157=CIRCLE ( 'NONE', #183, 2.055000000000000160 ) ;
#1161=AXIS2_PLACEMENT_3D ( 'NONE', #312, #1164, #2210 ) ;
#1164=DIRECTION ( 'NONE',  ( -1.000000000000000000, -0.000000000000000000, -0.000000000000000000 ) ) ;
#1165=VERTEX_POINT ( 'NONE', #1404 ) ;
#1168=EDGE_CURVE ( 'NONE', #463, #1097, #316, .T. ) ;
#1173=AXIS2_PLACEMENT_3D ( 'NONE', #301, #990, #649 ) ;
#1177=ORIENTED_EDGE ( 'NONE', *, *, #384, .F. ) ;
#1179=AXIS2_PLACEMENT_3D ( 'NONE', #1881, #1888, #900 ) ;
#1182=( NAMED_UNIT ( * ) SI_UNIT ( $, .STERADIAN. ) SOLID_ANGLE_UNIT ( ) );
#1187=CARTESIAN_POINT ( 'NONE',  ( 5.200000000000002842, 0.000000000000000000, 0.000000000000000000 ) ) ;
#1198=FACE_OUTER_BOUND ( 'NONE', #411, .T. ) ;
#1200=EDGE_LOOP ( 'NONE', ( #1949, #123, #881, #1613, #1745 ) ) ;
#1202=ORIENTED_EDGE ( 'NONE', *, *, #616, .F. ) ;
#1206=AXIS2_PLACEMENT_3D ( 'NONE', #1699, #852, #1386 ) ;
#1207=CARTESIAN_POINT ( 'NONE',  ( 0.000000000000000000, -1.178949249685218748, -2.041999999999998039 ) ) ;
#1208=ADVANCED_FACE ( 'NONE', ( #1198 ), #673, .F. ) ;
#1211=DIRECTION ( 'NONE',  ( 0.000000000000000000, 0.000000000000000000, 1.000000000000000000 ) ) ;
#1212=DIRECTION ( 'NONE',  ( 0.000000000000000000, 0.4999999999999992784, -0.8660254037844389297 ) ) ;
#1216=VECTOR ( 'NONE', #371, 999.9999999999997726 ) ;
#1221=FACE_OUTER_BOUND ( 'NONE', #715, .T. ) ;
#1224=CIRCLE ( 'NONE', #624, 4.250000000000000000 ) ;
#1226=ADVANCED_BREP_SHAPE_REPRESENTATION ( '', ( #1685, #30 ), #1018 ) ;
#1231=ORIENTED_EDGE ( 'NONE', *, *, #765, .F. ) ;
#1232=FACE_OUTER_BOUND ( 'NONE', #2085, .T. ) ;
#1234=LINE ( 'NONE', #1918, #1799 ) ;
#1235=LINE ( 'NONE', #711, #338 ) ;
#1238=CARTESIAN_POINT ( 'NONE',  ( 2.500000000000000000, 2.357898499370431722, -2.818925648462311528E-15 ) ) ;
#1247=DIRECTION ( 'NONE',  ( 0.000000000000000000, 0.000000000000000000, -1.000000000000000000 ) ) ;
#1250=AXIS2_PLACEMENT_3D ( 'NONE', #439, #1118, #1801 ) ;
#1252=AXIS2_PLACEMENT_3D ( 'NONE', #149, #1020, #1319 ) ;
#1254=ORIENTED_EDGE ( 'NONE', *, *, #518, .F. ) ;
#1258=CARTESIAN_POINT ( 'NONE',  ( 5.200000000000002842, 3.306546357697854226E-16, 2.700000000000000622 ) ) ;
#1259=ADVANCED_FACE ( 'NONE', ( #690 ), #1556, .T. ) ;
#1260=CARTESIAN_POINT ( 'NONE',  ( 21.00000000000000355, 0.000000000000000000, 2.055000000000000160 ) ) ;
#1261=VECTOR ( 'NONE', #1655, 1000.000000000000114 ) ;
#1263=FACE_OUTER_BOUND ( 'NONE', #349, .T. ) ;
#1264=AXIS2_PLACEMENT_3D ( 'NONE', #1273, #1954, #1296 ) ;
#1266=EDGE_LOOP ( 'NONE', ( #994, #322, #1098, #688, #1580 ) ) ;
#1267=ADVANCED_FACE ( 'NONE', ( #1368 ), #8, .T. ) ;
#1271=CARTESIAN_POINT ( 'NONE',  ( 0.000000000000000000, -1.178949249685214307, 2.042000000000001592 ) ) ;
#1273=CARTESIAN_POINT ( 'NONE',  ( 20.55500000000001748, 0.000000000000000000, 0.000000000000000000 ) ) ;
#1274=CYLINDRICAL_SURFACE ( 'NONE', #2189, 4.250000000000000000 ) ;
#1283=CARTESIAN_POINT ( 'NONE',  ( 21.00000000000000000, 2.055000000000000160, 0.000000000000000000 ) ) ;
#1285=CIRCLE ( 'NONE', #1105, 4.250000000000000000 ) ;
#1290=ORIENTED_EDGE ( 'NONE', *, *, #1143, .F. ) ;
#1292=CARTESIAN_POINT ( 'NONE',  ( 2.500000000000000000, -2.629050547790028551E-15, -2.041999999999999815 ) ) ;
#1295=ORIENTED_EDGE ( 'NONE', *, *, #880, .F. ) ;
#1296=DIRECTION ( 'NONE',  ( 0.000000000000000000, 0.000000000000000000, 1.000000000000000000 ) ) ;
#1307=DIRECTION ( 'NONE',  ( 0.000000000000000000, 0.000000000000000000, -1.000000000000000000 ) ) ;
#1308=CARTESIAN_POINT ( 'NONE',  ( 2.500000000000000000, 2.357898499370431722, -2.818925648462311528E-15 ) ) ;
#1309=EDGE_CURVE ( 'NONE', #1470, #226, #856, .T. ) ;
#1311=( LENGTH_UNIT ( ) NAMED_UNIT ( * ) SI_UNIT ( .MILLI., .METRE. ) );
#1319=DIRECTION ( 'NONE',  ( 0.000000000000000000, 0.000000000000000000, 1.000000000000000000 ) ) ;
#1321=AXIS2_PLACEMENT_3D ( 'NONE', #1283, #382, #1307 ) ;
#1335=PLANE ( 'NONE',  #1585 ) ;
#1340=CIRCLE ( 'NONE', #1021, 2.700000000000000622 ) ;
#1341=ORIENTED_EDGE ( 'NONE', *, *, #2196, .F. ) ;
#1342=DIRECTION ( 'NONE',  ( 0.000000000000000000, 0.000000000000000000, 1.000000000000000000 ) ) ;
#1343=ORIENTED_EDGE ( 'NONE', *, *, #232, .F. ) ;
#1344=EDGE_CURVE ( 'NONE', #1831, #1569, #948, .T. ) ;
#1347=ADVANCED_FACE ( 'NONE', ( #1433, #1089 ), #1614, .T. ) ;
#1348=VERTEX_POINT ( 'NONE', #58 ) ;
#1353=VERTEX_POINT ( 'NONE', #562 ) ;
#1355=CARTESIAN_POINT ( 'NONE',  ( 0.000000000000000000, 2.357898499370431722, -2.818925648462311528E-15 ) ) ;
#1357=UNCERTAINTY_MEASURE_WITH_UNIT (LENGTH_MEASURE( 1.000000000000000082E-05 ), #618, 'distance_accuracy_value', 'NONE');
#1358=VERTEX_POINT ( 'NONE', #1416 ) ;
#1360=CIRCLE ( 'NONE', #1420, 0.2500000000000002220 ) ;
#1362=FILL_AREA_STYLE ('',( #2225 ) ) ;
#1363=EDGE_CURVE ( 'NONE', #405, #2192, #233, .T. ) ;
#1364=EDGE_LOOP ( 'NONE', ( #442, #915, #824, #454, #452 ) ) ;
#1368=FACE_OUTER_BOUND ( 'NONE', #140, .T. ) ;
#1369=VECTOR ( 'NONE', #851, 1000.000000000000000 ) ;
#1373=ADVANCED_FACE ( 'NONE', ( #753 ), #1425, .F. ) ;
#1374=ORIENTED_EDGE ( 'NONE', *, *, #1767, .F. ) ;
#1375=ORIENTED_EDGE ( 'NONE', *, *, #1363, .T. ) ;
#1376=CIRCLE ( 'NONE', #406, 2.041999999999999815 ) ;
#1380=ADVANCED_FACE ( 'NONE', ( #400 ), #1112, .F. ) ;
#1381=( LENGTH_UNIT ( ) NAMED_UNIT ( * ) SI_UNIT ( .MILLI., .METRE. ) );
#1384=ORIENTED_EDGE ( 'NONE', *, *, #746, .T. ) ;
#1386=DIRECTION ( 'NONE',  ( 0.000000000000000000, 0.000000000000000000, 1.000000000000000000 ) ) ;
#1398=CONICAL_SURFACE ( 'NONE', #1719, 2.055000000000000160, 0.7853981633974639331 ) ;
#1399=PLANE ( 'NONE',  #1435 ) ;
#1402=ORIENTED_EDGE ( 'NONE', *, *, #1103, .F. ) ;
#1404=CARTESIAN_POINT ( 'NONE',  ( 2.500000000000000000, -1.768423874527823569, 1.021000000000002350 ) ) ;
#1407=AXIS2_PLACEMENT_3D ( 'NONE', #200, #692, #720 ) ;
#1408=AXIS2_PLACEMENT_3D ( 'NONE', #609, #1966, #1079 ) ;
#1410=PRODUCT_DEFINITION ( 'UNKNOWN', '', #836, #2052 ) ;
#1412=CARTESIAN_POINT ( 'NONE',  ( 0.2500000000000002220, 0.000000000000000000, 4.250000000000000000 ) ) ;
#1416=CARTESIAN_POINT ( 'NONE',  ( 21.00000000000000355, 0.000000000000000000, 2.055000000000000160 ) ) ;
#1417=FACE_OUTER_BOUND ( 'NONE', #1266, .T. ) ;
#1418=CARTESIAN_POINT ( 'NONE',  ( 0.000000000000000000, 1.178949249685217415, 2.041999999999998483 ) ) ;
#1420=AXIS2_PLACEMENT_3D ( 'NONE', #1099, #1780, #1088 ) ;
#1425=PLANE ( 'NONE',  #685 ) ;
#1429=CIRCLE ( 'NONE', #1148, 2.055000000000000160 ) ;
#1433=FACE_BOUND ( 'NONE', #871, .T. ) ;
#1435=AXIS2_PLACEMENT_3D ( 'NONE', #239, #85, #961 ) ;
#1437=CARTESIAN_POINT ( 'NONE',  ( 0.000000000000000000, 2.357898499370431722, -2.818925648462311528E-15 ) ) ;
#1438=ORIENTED_EDGE ( 'NONE', *, *, #1751, .T. ) ;
#1452=ORIENTED_EDGE ( 'NONE', *, *, #384, .T. ) ;
#1453=VECTOR ( 'NONE', #435, 1000.000000000000114 ) ;
#1455=LINE ( 'NONE', #1271, #480 ) ;
#1456=ORIENTED_EDGE ( 'NONE', *, *, #55, .F. ) ;
#1457=DIRECTION ( 'NONE',  ( 0.000000000000000000, 0.000000000000000000, 1.000000000000000000 ) ) ;
#1467=DIRECTION ( 'NONE',  ( -0.7071067811865364705, 8.659560562355067211E-17, -0.7071067811865584529 ) ) ;
#1470=VERTEX_POINT ( 'NONE', #602 ) ;
#1481=EDGE_LOOP ( 'NONE', ( #1102, #364, #133, #1008 ) ) ;
#1484=DIRECTION ( 'NONE',  ( 0.000000000000000000, 1.000000000000000000, -1.287488025362403787E-15 ) ) ;
#1494=LINE ( 'NONE', #1653, #1930 ) ;
#1497=DIRECTION ( 'NONE',  ( 0.000000000000000000, 0.000000000000000000, -1.000000000000000000 ) ) ;
#1500=ADVANCED_FACE ( 'NONE', ( #1263 ), #1274, .T. ) ;
#1505=VERTEX_POINT ( 'NONE', #1437 ) ;
#1506=STYLED_ITEM('',(#2268),#1685);
#1507=LINE ( 'NONE', #1355, #1063 ) ;
#1511=CARTESIAN_POINT ( 'NONE',  ( 2.500000000000000000, 0.000000000000000000, 0.000000000000000000 ) ) ;
#1517=ORIENTED_EDGE ( 'NONE', *, *, #1850, .T. ) ;
#1520=ORIENTED_EDGE ( 'NONE', *, *, #13, .T. ) ;
#1522=CARTESIAN_POINT ( 'NONE',  ( 2.500000000000000000, 2.357898499370431722, -2.818925648462311528E-15 ) ) ;
#1524=ORIENTED_EDGE ( 'NONE', *, *, #706, .F. ) ;
#1529=UNCERTAINTY_MEASURE_WITH_UNIT (LENGTH_MEASURE( 1.000000000000000082E-05 ), #1311, 'distance_accuracy_value', 'NONE');
#1533=CIRCLE ( 'NONE', #2037, 2.500000000000000444 ) ;
#1537=EDGE_LOOP ( 'NONE', ( #1810, #1202, #729, #558, #1384 ) ) ;
#1539=CARTESIAN_POINT ( 'NONE',  ( 2.500000000000000000, 0.000000000000000000, 0.000000000000000000 ) ) ;
#1541=VECTOR ( 'NONE', #1067, 1000.000000000000000 ) ;
#1543=ORIENTED_EDGE ( 'NONE', *, *, #1850, .F. ) ;
#1546=ADVANCED_FACE ( 'NONE', ( #757 ), #1398, .T. ) ;
#1548=SURFACE_STYLE_USAGE ( .BOTH. , #143 ) ;
#1549=STYLED_ITEM ( 'NONE', ( #319 ), #1226 ) ;
#1551=VECTOR ( 'NONE', #201, 1000.000000000000000 ) ;
#1552=ORIENTED_EDGE ( 'NONE', *, *, #993, .F. ) ;
#1556=PLANE ( 'NONE',  #274 ) ;
#1558=( NAMED_UNIT ( * ) PLANE_ANGLE_UNIT ( ) SI_UNIT ( $, .RADIAN. ) );
#1560=ADVANCED_FACE ( 'NONE', ( #968, #1647 ), #938, .T. ) ;
#1561=DIRECTION ( 'NONE',  ( -1.000000000000000000, -0.000000000000000000, -0.000000000000000000 ) ) ;
#1562=ADVANCED_FACE ( 'NONE', ( #1811 ), #750, .F. ) ;
#1566=CARTESIAN_POINT ( 'NONE',  ( 2.500000000000000000, 0.000000000000000000, 2.041999999999999815 ) ) ;
#1569=VERTEX_POINT ( 'NONE', #556 ) ;
#1572=LINE ( 'NONE', #196, #926 ) ;
#1579=VERTEX_POINT ( 'NONE', #1412 ) ;
#1580=ORIENTED_EDGE ( 'NONE', *, *, #40, .T. ) ;
#1581=DIRECTION ( 'NONE',  ( 0.000000000000000000, 0.000000000000000000, -1.000000000000000000 ) ) ;
#1583=DIRECTION ( 'NONE',  ( 0.000000000000000000, 1.224646799147353207E-16, 1.000000000000000000 ) ) ;
#1584=VECTOR ( 'NONE', #295, 1000.000000000000114 ) ;
#1585=AXIS2_PLACEMENT_3D ( 'NONE', #844, #1001, #820 ) ;
#1591=DIRECTION ( 'NONE',  ( 0.000000000000000000, -1.000000000000000000, 1.287488025362403787E-15 ) ) ;
#1592=DIRECTION ( 'NONE',  ( 0.000000000000000000, 0.000000000000000000, -1.000000000000000000 ) ) ;
#1598=CARTESIAN_POINT ( 'NONE',  ( 0.000000000000000000, 5.051668046482832750E-16, -4.000000000000000000 ) ) ;
#1604=DIRECTION ( 'NONE',  ( 0.000000000000000000, 1.000000000000000000, -1.224646799147353207E-16 ) ) ;
#1607=ADVANCED_FACE ( 'NONE', ( #2071 ), #578, .T. ) ;
#1613=ORIENTED_EDGE ( 'NONE', *, *, #2212, .T. ) ;
#1614=PLANE ( 'NONE',  #570 ) ;
#1616=CARTESIAN_POINT ( 'NONE',  ( 20.55500000000001748, 0.000000000000000000, 2.500000000000000888 ) ) ;
#1617=EDGE_LOOP ( 'NONE', ( #2222, #755, #815 ) ) ;
#1618=VECTOR ( 'NONE', #2171, 1000.000000000000000 ) ;
#1619=VECTOR ( 'NONE', #2007, 1000.000000000000000 ) ;
#1623=DIRECTION ( 'NONE',  ( 0.000000000000000000, 0.000000000000000000, 1.000000000000000000 ) ) ;
#1625=VERTEX_POINT ( 'NONE', #535 ) ;
#1626=ORIENTED_EDGE ( 'NONE', *, *, #1168, .T. ) ;
#1629=ORIENTED_EDGE ( 'NONE', *, *, #180, .T. ) ;
#1631=VERTEX_POINT ( 'NONE', #212 ) ;
#1633=CARTESIAN_POINT ( 'NONE',  ( -31.74999999999995737, 0.000000000000000000, 0.000000000000000000 ) ) ;
#1636=ORIENTED_EDGE ( 'NONE', *, *, #2015, .F. ) ;
#1640=DIRECTION ( 'NONE',  ( -1.000000000000000000, -0.000000000000000000, -0.000000000000000000 ) ) ;
#1641=ORIENTED_EDGE ( 'NONE', *, *, #1992, .F. ) ;
#1643=DIRECTION ( 'NONE',  ( -1.000000000000000000, -0.000000000000000000, -0.000000000000000000 ) ) ;
#1647=FACE_OUTER_BOUND ( 'NONE', #950, .T. ) ;
#1650=ORIENTED_EDGE ( 'NONE', *, *, #879, .T. ) ;
#1651=CARTESIAN_POINT ( 'NONE',  ( 0.000000000000000000, 1.178949249685212974, -2.042000000000001148 ) ) ;
#1653=CARTESIAN_POINT ( 'NONE',  ( 2.500000000000000000, -1.178949249685218748, -2.041999999999998039 ) ) ;
#1654=DIRECTION ( 'NONE',  ( 0.000000000000000000, 0.4999999999999990008, -0.8660254037844391517 ) ) ;
#1655=DIRECTION ( 'NONE',  ( 0.000000000000000000, 0.4999999999999990008, -0.8660254037844391517 ) ) ;
#1660=DIRECTION ( 'NONE',  ( 0.000000000000000000, 0.000000000000000000, 1.000000000000000000 ) ) ;
#1665=CARTESIAN_POINT ( 'NONE',  ( 0.000000000000000000, -2.357898499370432166, 3.035766082959412415E-15 ) ) ;
#1672=VERTEX_POINT ( 'NONE', #1598 ) ;
#1675=DIRECTION ( 'NONE',  ( 0.000000000000000000, 0.000000000000000000, -1.000000000000000000 ) ) ;
#1676=PLANE ( 'NONE',  #1904 ) ;
#1679=DIRECTION ( 'NONE',  ( 0.000000000000000000, 0.000000000000000000, 1.000000000000000000 ) ) ;
#1681=EDGE_CURVE ( 'NONE', #830, #65, #193, .T. ) ;
#1684=EDGE_LOOP ( 'NONE', ( #1375, #661, #1438, #1231 ) ) ;
#1685=MANIFOLD_SOLID_BREP ( 'Hex', #290 ) ;
#1686=MECHANICAL_DESIGN_GEOMETRIC_PRESENTATION_REPRESENTATION('',(#1506),#972);
#1698=CARTESIAN_POINT ( 'NONE',  ( 2.500000000000000000, 2.357898499370431722, -2.818925648462311528E-15 ) ) ;
#1699=CARTESIAN_POINT ( 'NONE',  ( 20.55500000000001748, 0.000000000000000000, 0.000000000000000000 ) ) ;
#1708=EDGE_CURVE ( 'NONE', #1569, #957, #799, .T. ) ;
#1710=DIRECTION ( 'NONE',  ( 0.000000000000000000, 0.000000000000000000, 1.000000000000000000 ) ) ;
#1712=EDGE_CURVE ( 'NONE', #1631, #776, #810, .T. ) ;
#1719=AXIS2_PLACEMENT_3D ( 'NONE', #1776, #413, #2152 ) ;
#1724=AXIS2_PLACEMENT_3D ( 'NONE', #504, #153, #141 ) ;
#1729=LINE ( 'NONE', #894, #1120 ) ;
#1730=ADVANCED_FACE ( 'NONE', ( #1141 ), #1967, .T. ) ;
#1738=CARTESIAN_POINT ( 'NONE',  ( 2.500000000000000000, -1.178949249685218748, -2.041999999999998039 ) ) ;
#1739=VECTOR ( 'NONE', #1654, 1000.000000000000114 ) ;
#1743=CARTESIAN_POINT ( 'NONE',  ( -31.74999999999995737, 5.204748896376250699E-16, -4.250000000000000000 ) ) ;
#1744=DIRECTION ( 'NONE',  ( 0.000000000000000000, 0.8660254037844380415, -0.5000000000000009992 ) ) ;
#1745=ORIENTED_EDGE ( 'NONE', *, *, #1103, .T. ) ;
#1751=EDGE_CURVE ( 'NONE', #4, #1579, #1285, .T. ) ;
#1757=ORIENTED_EDGE ( 'NONE', *, *, #1344, .T. ) ;
#1761=DIRECTION ( 'NONE',  ( -0.000000000000000000, 1.287488025362403787E-15, 1.000000000000000000 ) ) ;
#1763=EDGE_LOOP ( 'NONE', ( #2058, #1979, #1032 ) ) ;
#1764=DIRECTION ( 'NONE',  ( -1.000000000000000000, -0.000000000000000000, -0.000000000000000000 ) ) ;
#1765=DIRECTION ( 'NONE',  ( 0.000000000000000000, 0.000000000000000000, 1.000000000000000000 ) ) ;
#1766=ORIENTED_EDGE ( 'NONE', *, *, #1034, .T. ) ;
#1767=EDGE_CURVE ( 'NONE', #1165, #575, #2148, .T. ) ;
#1768=EDGE_LOOP ( 'NONE', ( #1290, #1124, #2128 ) ) ;
#1770=DIRECTION ( 'NONE',  ( -0.000000000000000000, 0.000000000000000000, 1.000000000000000000 ) ) ;
#1774=AXIS2_PLACEMENT_3D ( 'NONE', #1539, #525, #1710 ) ;
#1775=ADVANCED_FACE ( 'NONE', ( #1221 ), #1872, .F. ) ;
#1776=CARTESIAN_POINT ( 'NONE',  ( 21.00000000000000355, 0.000000000000000000, 0.000000000000000000 ) ) ;
#1779=ORIENTED_EDGE ( 'NONE', *, *, #2000, .F. ) ;
#1780=DIRECTION ( 'NONE',  ( -0.000000000000000000, 1.000000000000000000, 1.224646799147353207E-16 ) ) ;
#1786=DIRECTION ( 'NONE',  ( 1.000000000000000000, 0.000000000000000000, 0.000000000000000000 ) ) ;
#1787=AXIS2_PLACEMENT_3D ( 'NONE', #547, #1744, #11 ) ;
#1794=VERTEX_POINT ( 'NONE', #164 ) ;
#1795=LINE ( 'NONE', #1238, #1892 ) ;
#1796=ORIENTED_EDGE ( 'NONE', *, *, #2000, .T. ) ;
#1797=DIRECTION ( 'NONE',  ( 0.000000000000000000, -1.287488025362403787E-15, -1.000000000000000000 ) ) ;
#1799=VECTOR ( 'NONE', #992, 1000.000000000000000 ) ;
#1801=DIRECTION ( 'NONE',  ( 0.000000000000000000, 0.000000000000000000, 1.000000000000000000 ) ) ;
#1804=EDGE_CURVE ( 'NONE', #1470, #1794, #139, .T. ) ;
#1805=ORIENTED_EDGE ( 'NONE', *, *, #746, .F. ) ;
#1808=EDGE_LOOP ( 'NONE', ( #1254, #1650, #1452, #195 ) ) ;
#1809=DIRECTION ( 'NONE',  ( 0.000000000000000000, -0.5000000000000013323, -0.8660254037844380415 ) ) ;
#1810=ORIENTED_EDGE ( 'NONE', *, *, #144, .T. ) ;
#1811=FACE_OUTER_BOUND ( 'NONE', #1200, .T. ) ;
#1813=AXIS2_PLACEMENT_3D ( 'NONE', #2051, #699, #1212 ) ;
#1816=VERTEX_POINT ( 'NONE', #1738 ) ;
#1822=DIRECTION ( 'NONE',  ( 0.000000000000000000, 0.000000000000000000, -1.000000000000000000 ) ) ;
#1830=CARTESIAN_POINT ( 'NONE',  ( 2.500000000000000000, -1.178949249685214307, 2.042000000000001592 ) ) ;
#1831=VERTEX_POINT ( 'NONE', #1849 ) ;
#1833=CARTESIAN_POINT ( 'NONE',  ( 20.55500000000001748, 3.061616997868384127E-16, -2.500000000000000888 ) ) ;
#1836=CARTESIAN_POINT ( 'NONE',  ( 0.2500000000000002220, 0.000000000000000000, 0.000000000000000000 ) ) ;
#1845=FACE_OUTER_BOUND ( 'NONE', #270, .T. ) ;
#1849=CARTESIAN_POINT ( 'NONE',  ( 2.500000000000000000, 1.768423874527823791, 1.020999999999998353 ) ) ;
#1850=EDGE_CURVE ( 'NONE', #776, #1165, #895, .T. ) ;
#1855=ORIENTED_EDGE ( 'NONE', *, *, #1973, .F. ) ;
#1856=VECTOR ( 'NONE', #192, 1000.000000000000000 ) ;
#1858=LINE ( 'NONE', #1665, #1739 ) ;
#1868=DIRECTION ( 'NONE',  ( 1.000000000000000000, 0.000000000000000000, 0.000000000000000000 ) ) ;
#1869=UNCERTAINTY_MEASURE_WITH_UNIT (LENGTH_MEASURE( 1.000000000000000082E-05 ), #1381, 'distance_accuracy_value', 'NONE');
#1871=CARTESIAN_POINT ( 'NONE',  ( 2.500000000000000000, -1.178949249685214307, 2.042000000000001592 ) ) ;
#1872=PLANE ( 'NONE',  #286 ) ;
#1873=SHAPE_REPRESENTATION_RELATIONSHIP ( 'NONE' , 'NONE' ,  #354, #1226 ) ;
#1874=CIRCLE ( 'NONE', #2018, 2.041999999999999815 ) ;
#1880=EDGE_LOOP ( 'NONE', ( #769, #975, #1981, #1936 ) ) ;
#1881=CARTESIAN_POINT ( 'NONE',  ( -31.74999999999995737, 0.000000000000000000, 0.000000000000000000 ) ) ;
#1888=DIRECTION ( 'NONE',  ( -1.000000000000000000, -0.000000000000000000, -0.000000000000000000 ) ) ;
#1892=VECTOR ( 'NONE', #1809, 999.9999999999997726 ) ;
#1894=AXIS2_PLACEMENT_3D ( 'NONE', #2109, #587, #1952 ) ;
#1896=LINE ( 'NONE', #891, #91 ) ;
#1902=VECTOR ( 'NONE', #1484, 1000.000000000000000 ) ;
#1904=AXIS2_PLACEMENT_3D ( 'NONE', #150, #2195, #1822 ) ;
#1905=VECTOR ( 'NONE', #764, 1000.000000000000114 ) ;
#1914=ORIENTED_EDGE ( 'NONE', *, *, #1681, .T. ) ;
#1918=CARTESIAN_POINT ( 'NONE',  ( 2.500000000000000000, -1.178949249685214307, 2.042000000000001592 ) ) ;
#1919=AXIS2_PLACEMENT_3D ( 'NONE', #2027, #660, #2172 ) ;
#1925=ORIENTED_EDGE ( 'NONE', *, *, #1007, .T. ) ;
#1927=DIRECTION ( 'NONE',  ( -1.000000000000000000, 0.000000000000000000, -0.000000000000000000 ) ) ;
#1930=VECTOR ( 'NONE', #325, 1000.000000000000000 ) ;
#1932=AXIS2_PLACEMENT_3D ( 'NONE', #614, #1986, #1131 ) ;
#1935=EDGE_CURVE ( 'NONE', #1625, #575, #1234, .T. ) ;
#1936=ORIENTED_EDGE ( 'NONE', *, *, #1309, .F. ) ;
#1939=ORIENTED_EDGE ( 'NONE', *, *, #2166, .F. ) ;
#1949=ORIENTED_EDGE ( 'NONE', *, *, #165, .F. ) ;
#1950=ORIENTED_EDGE ( 'NONE', *, *, #765, .T. ) ;
#1952=DIRECTION ( 'NONE',  ( 0.000000000000000000, 0.5000000000000011102, 0.8660254037844379305 ) ) ;
#1953=CARTESIAN_POINT ( 'NONE',  ( 5.000000000000000888, 0.000000000000000000, 0.000000000000000000 ) ) ;
#1954=DIRECTION ( 'NONE',  ( -1.000000000000000000, -0.000000000000000000, -0.000000000000000000 ) ) ;
#1956=EDGE_CURVE ( 'NONE', #1165, #1631, #563, .T. ) ;
#1958=CARTESIAN_POINT ( 'NONE',  ( 0.2500000000000002220, 0.000000000000000000, 0.000000000000000000 ) ) ;
#1966=DIRECTION ( 'NONE',  ( -1.000000000000000000, -0.000000000000000000, -0.000000000000000000 ) ) ;
#1967=TOROIDAL_SURFACE ( 'NONE', #2224, 4.000000000000000000, 0.2500000000000000000 ) ;
#1968=CARTESIAN_POINT ( 'NONE',  ( -31.74999999999995737, 0.000000000000000000, 2.500000000000000444 ) ) ;
#1973=EDGE_CURVE ( 'NONE', #1794, #627, #444, .T. ) ;
#1974=DIRECTION ( 'NONE',  ( -1.000000000000000000, -0.000000000000000000, -0.000000000000000000 ) ) ;
#1975=ORIENTED_EDGE ( 'NONE', *, *, #1168, .F. ) ;
#1978=LINE ( 'NONE', #2180, #34 ) ;
#1979=ORIENTED_EDGE ( 'NONE', *, *, #1344, .F. ) ;
#1980=CARTESIAN_POINT ( 'NONE',  ( -31.74999999999995737, 3.061616997868383634E-16, -2.500000000000000444 ) ) ;
#1981=ORIENTED_EDGE ( 'NONE', *, *, #180, .F. ) ;
#1984=CIRCLE ( 'NONE', #1161, 4.000000000000000000 ) ;
#1986=DIRECTION ( 'NONE',  ( 1.000000000000000000, 0.000000000000000000, 0.000000000000000000 ) ) ;
#1987=DIRECTION ( 'NONE',  ( 0.000000000000000000, 0.4999999999999990008, -0.8660254037844391517 ) ) ;
#1991=DIRECTION ( 'NONE',  ( 0.000000000000000000, -0.4999999999999993339, 0.8660254037844390407 ) ) ;
#1992=EDGE_CURVE ( 'NONE', #1348, #957, #1455, .T. ) ;
#1994=PLANE ( 'NONE',  #1321 ) ;
#1995=DIRECTION ( 'NONE',  ( 0.000000000000000000, -0.4999999999999993339, 0.8660254037844390407 ) ) ;
#1996=LINE ( 'NONE', #2214, #1261 ) ;
#1997=( NAMED_UNIT ( * ) PLANE_ANGLE_UNIT ( ) SI_UNIT ( $, .RADIAN. ) );
#2000=EDGE_CURVE ( 'NONE', #627, #226, #1340, .T. ) ;
#2005=FACE_OUTER_BOUND ( 'NONE', #1481, .T. ) ;
#2007=DIRECTION ( 'NONE',  ( -1.000000000000000000, -0.000000000000000000, -0.000000000000000000 ) ) ;
#2012=ORIENTED_EDGE ( 'NONE', *, *, #2122, .F. ) ;
#2015=EDGE_CURVE ( 'NONE', #2192, #405, #840, .T. ) ;
#2017=DIRECTION ( 'NONE',  ( 0.000000000000000000, 0.000000000000000000, 1.000000000000000000 ) ) ;
#2018=AXIS2_PLACEMENT_3D ( 'NONE', #464, #1640, #1342 ) ;
#2022=AXIS2_PLACEMENT_3D ( 'NONE', #1258, #1604, #1583 ) ;
#2023=ORIENTED_EDGE ( 'NONE', *, *, #993, .T. ) ;
#2026=LINE ( 'NONE', #2050, #1618 ) ;
#2027=CARTESIAN_POINT ( 'NONE',  ( 21.00000000000000355, 0.000000000000000000, 0.000000000000000000 ) ) ;
#2029=CARTESIAN_POINT ( 'NONE',  ( 2.500000000000000000, 2.629050547790028946E-15, 2.042000000000000259 ) ) ;
#2030=DIRECTION ( 'NONE',  ( 0.000000000000000000, 0.000000000000000000, -1.000000000000000000 ) ) ;
#2032=VECTOR ( 'NONE', #1995, 1000.000000000000000 ) ;
#2035=EDGE_LOOP ( 'NONE', ( #2023, #909 ) ) ;
#2037=AXIS2_PLACEMENT_3D ( 'NONE', #189, #207, #1581 ) ;
#2050=CARTESIAN_POINT ( 'NONE',  ( 2.500000000000000000, -2.357898499370432166, 3.035766082959412415E-15 ) ) ;
#2051=CARTESIAN_POINT ( 'NONE',  ( 2.500000000000000000, 2.357898499370431722, -2.818925648462311528E-15 ) ) ;
#2052=PRODUCT_DEFINITION_CONTEXT ( 'detailed design', #431, 'design' ) ;
#2053=VERTEX_POINT ( 'NONE', #1292 ) ;
#2057=CIRCLE ( 'NONE', #1264, 2.500000000000000888 ) ;
#2058=ORIENTED_EDGE ( 'NONE', *, *, #670, .T. ) ;
#2059=ORIENTED_EDGE ( 'NONE', *, *, #1712, .T. ) ;
#2060=DIRECTION ( 'NONE',  ( -1.000000000000000000, -0.000000000000000000, -0.000000000000000000 ) ) ;
#2065=AXIS2_PLACEMENT_3D ( 'NONE', #608, #731, #1592 ) ;
#2066=ORIENTED_EDGE ( 'NONE', *, *, #1143, .T. ) ;
#2068=CARTESIAN_POINT ( 'NONE',  ( 5.000000000000000888, 0.000000000000000000, 0.000000000000000000 ) ) ;
#2071=FACE_OUTER_BOUND ( 'NONE', #1364, .T. ) ;
#2081=CYLINDRICAL_SURFACE ( 'NONE', #1, 2.500000000000000444 ) ;
#2083=EDGE_CURVE ( 'NONE', #1625, #1165, #666, .T. ) ;
#2085=EDGE_LOOP ( 'NONE', ( #1626, #136, #515, #1177 ) ) ;
#2086=VECTOR ( 'NONE', #743, 1000.000000000000114 ) ;
#2089=CARTESIAN_POINT ( 'NONE',  ( 2.500000000000000000, 2.357898499370431722, -2.818925648462311528E-15 ) ) ;
#2092=CARTESIAN_POINT ( 'NONE',  ( 21.00000000000000355, 0.000000000000000000, 0.000000000000000000 ) ) ;
#2099=CARTESIAN_POINT ( 'NONE',  ( 4.999999999999997335, 0.000000000000000000, 0.000000000000000000 ) ) ;
#2100=PLANE ( 'NONE',  #156 ) ;
#2101=DIRECTION ( 'NONE',  ( 0.000000000000000000, 0.000000000000000000, 1.000000000000000000 ) ) ;
#2103=ADVANCED_FACE ( 'NONE', ( #1417 ), #2100, .F. ) ;
#2109=CARTESIAN_POINT ( 'NONE',  ( 2.500000000000000000, 2.357898499370431722, -2.818925648462311528E-15 ) ) ;
#2115=CARTESIAN_POINT ( 'NONE',  ( 0.2500000000000002220, 5.204748896376250699E-16, -4.250000000000000000 ) ) ;
#2119=DIRECTION ( 'NONE',  ( 1.000000000000000000, 0.000000000000000000, 0.000000000000000000 ) ) ;
#2122=EDGE_CURVE ( 'NONE', #1505, #957, #1978, .T. ) ;
#2123=AXIS2_PLACEMENT_3D ( 'NONE', #1187, #1868, #468 ) ;
#2127=CARTESIAN_POINT ( 'NONE',  ( 2.500000000000000000, -2.357898499370432166, 3.035766082959412415E-15 ) ) ;
#2128=ORIENTED_EDGE ( 'NONE', *, *, #2212, .F. ) ;
#2135=EDGE_LOOP ( 'NONE', ( #1855, #54, #503, #1779 ) ) ;
#2146=DIRECTION ( 'NONE',  ( -1.000000000000000000, -0.000000000000000000, -0.000000000000000000 ) ) ;
#2148=CIRCLE ( 'NONE', #1250, 2.041999999999999815 ) ;
#2152=DIRECTION ( 'NONE',  ( 0.000000000000000000, 0.000000000000000000, 1.000000000000000000 ) ) ;
#2157=LINE ( 'NONE', #1651, #255 ) ;
#2158=ORIENTED_EDGE ( 'NONE', *, *, #2196, .T. ) ;
#2166=EDGE_CURVE ( 'NONE', #1353, #1097, #814, .T. ) ;
#2171=DIRECTION ( 'NONE',  ( -1.000000000000000000, -0.000000000000000000, -0.000000000000000000 ) ) ;
#2172=DIRECTION ( 'NONE',  ( 0.000000000000000000, 0.000000000000000000, 1.000000000000000000 ) ) ;
#2180=CARTESIAN_POINT ( 'NONE',  ( 0.000000000000000000, 2.357898499370431722, -2.818925648462311528E-15 ) ) ;
#2189=AXIS2_PLACEMENT_3D ( 'NONE', #1633, #629, #76 ) ;
#2191=DIRECTION ( 'NONE',  ( 0.000000000000000000, -1.000000000000000000, 1.287488025362403787E-15 ) ) ;
#2192=VERTEX_POINT ( 'NONE', #959 ) ;
#2195=DIRECTION ( 'NONE',  ( 1.000000000000000000, 0.000000000000000000, 0.000000000000000000 ) ) ;
#2196=EDGE_CURVE ( 'NONE', #145, #847, #2157, .T. ) ;
#2200=DIRECTION ( 'NONE',  ( 0.000000000000000000, 0.000000000000000000, 1.000000000000000000 ) ) ;
#2203=( NAMED_UNIT ( * ) SI_UNIT ( $, .STERADIAN. ) SOLID_ANGLE_UNIT ( ) );
#2209=FACE_OUTER_BOUND ( 'NONE', #1763, .T. ) ;
#2210=DIRECTION ( 'NONE',  ( 0.000000000000000000, 0.000000000000000000, 1.000000000000000000 ) ) ;
#2212=EDGE_CURVE ( 'NONE', #1831, #830, #1874, .T. ) ;
#2214=CARTESIAN_POINT ( 'NONE',  ( 2.500000000000000000, -2.357898499370432166, 3.035766082959412415E-15 ) ) ;
#2220=PLANE ( 'NONE',  #1073 ) ;
#2222=ORIENTED_EDGE ( 'NONE', *, *, #318, .T. ) ;
#2224=AXIS2_PLACEMENT_3D ( 'NONE', #1836, #304, #591 ) ;
#2225=FILL_AREA_STYLE_COLOUR ( '', #620 ) ;
#2262=COLOUR_RGB('Black',0.12,0.14,0.17);
#2263=FILL_AREA_STYLE_COLOUR('',#2262);
#2264=FILL_AREA_STYLE('',(#2263));
#2265=SURFACE_STYLE_FILL_AREA(#2264);
#2266=SURFACE_SIDE_STYLE('',(#2265));
#2267=SURFACE_STYLE_USAGE(.BOTH.,#2266);
#2268=PRESENTATION_STYLE_ASSIGNMENT((#2267));
ENDSEC;
END-ISO-10303-21;
